ISO-10303-21;
HEADER;
/* Generated by software containing ST-Developer
 * from STEP Tools, Inc. (www.steptools.com) 
 */

FILE_DESCRIPTION(
/* description */ ('Four-bar parallelogram arm'),
/* implementation_level */ '2;1');

FILE_NAME(
/* name */ 'Pivot keeper (3).step',
/* time_stamp */ '2026-10-28T03:24:55-07:00',
/* author */ (''),
/* organization */ (''),
/* preprocessor_version */ 'ST-DEVELOPER v20.2',
/* originating_system */ 'Autodesk Translation Framework v15.17.0.0',
/* authorisation */ '');

FILE_SCHEMA (('AUTOMOTIVE_DESIGN { 1 0 10303 214 3 1 1 }'));
ENDSEC;

DATA;
#10=MECHANICAL_DESIGN_GEOMETRIC_PRESENTATION_REPRESENTATION('',(#678),#14512);
#570=SHAPE_REPRESENTATION_RELATIONSHIP('SRR','None',#14795,#620);
#620=ADVANCED_BREP_SHAPE_REPRESENTATION('',(#734),#14510);
#678=STYLED_ITEM('',(#15101),#734);
#734=MANIFOLD_SOLID_BREP('Body1',#7384);
#1003=FACE_BOUND('',#2291,.T.);
#1004=FACE_BOUND('',#2293,.T.);
#1188=PLANE('',#8890);
#1189=PLANE('',#8891);
#1600=FACE_OUTER_BOUND('',#2288,.T.);
#1601=FACE_OUTER_BOUND('',#2289,.T.);
#1602=FACE_OUTER_BOUND('',#2290,.T.);
#1603=FACE_OUTER_BOUND('',#2292,.T.);
#2288=EDGE_LOOP('',(#6638,#6639,#6640,#6641));
#2289=EDGE_LOOP('',(#6642,#6643,#6644,#6645));
#2290=EDGE_LOOP('',(#6646));
#2291=EDGE_LOOP('',(#6647));
#2292=EDGE_LOOP('',(#6648));
#2293=EDGE_LOOP('',(#6649));
#2680=LINE('',#14267,#3074);
#2681=LINE('',#14273,#3075);
#3074=VECTOR('',#11234,0.225000000000001);
#3075=VECTOR('',#11241,0.899999999999999);
#3533=CIRCLE('',#8885,0.225000000000001);
#3534=CIRCLE('',#8886,0.225000000000001);
#3535=CIRCLE('',#8888,0.899999999999999);
#3536=CIRCLE('',#8889,0.899999999999999);
#4101=VERTEX_POINT('',#14264);
#4102=VERTEX_POINT('',#14266);
#4103=VERTEX_POINT('',#14270);
#4104=VERTEX_POINT('',#14272);
#4950=EDGE_CURVE('',#4101,#4101,#3533,.T.);
#4951=EDGE_CURVE('',#4101,#4102,#2680,.T.);
#4952=EDGE_CURVE('',#4102,#4102,#3534,.T.);
#4953=EDGE_CURVE('',#4103,#4103,#3535,.T.);
#4954=EDGE_CURVE('',#4103,#4104,#2681,.T.);
#4955=EDGE_CURVE('',#4104,#4104,#3536,.T.);
#6638=ORIENTED_EDGE('',*,*,#4950,.F.);
#6639=ORIENTED_EDGE('',*,*,#4951,.T.);
#6640=ORIENTED_EDGE('',*,*,#4952,.T.);
#6641=ORIENTED_EDGE('',*,*,#4951,.F.);
#6642=ORIENTED_EDGE('',*,*,#4953,.F.);
#6643=ORIENTED_EDGE('',*,*,#4954,.T.);
#6644=ORIENTED_EDGE('',*,*,#4955,.T.);
#6645=ORIENTED_EDGE('',*,*,#4954,.F.);
#6646=ORIENTED_EDGE('',*,*,#4953,.T.);
#6647=ORIENTED_EDGE('',*,*,#4950,.T.);
#6648=ORIENTED_EDGE('',*,*,#4955,.F.);
#6649=ORIENTED_EDGE('',*,*,#4952,.F.);
#6902=CYLINDRICAL_SURFACE('',#8884,0.225000000000001);
#6903=CYLINDRICAL_SURFACE('',#8887,0.899999999999999);
#7305=ADVANCED_FACE('',(#1600),#6902,.F.);
#7306=ADVANCED_FACE('',(#1601),#6903,.T.);
#7307=ADVANCED_FACE('',(#1602,#1003),#1188,.T.);
#7308=ADVANCED_FACE('',(#1603,#1004),#1189,.F.);
#7384=CLOSED_SHELL('',(#7305,#7306,#7307,#7308));
#8883=AXIS2_PLACEMENT_3D('',#14262,#11228,#11229);
#8884=AXIS2_PLACEMENT_3D('',#14263,#11230,#11231);
#8885=AXIS2_PLACEMENT_3D('',#14265,#11232,#11233);
#8886=AXIS2_PLACEMENT_3D('',#14268,#11235,#11236);
#8887=AXIS2_PLACEMENT_3D('',#14269,#11237,#11238);
#8888=AXIS2_PLACEMENT_3D('',#14271,#11239,#11240);
#8889=AXIS2_PLACEMENT_3D('',#14274,#11242,#11243);
#8890=AXIS2_PLACEMENT_3D('',#14275,#11244,#11245);
#8891=AXIS2_PLACEMENT_3D('',#14276,#11246,#11247);
#11228=DIRECTION('axis',(0.,0.,1.));
#11229=DIRECTION('refdir',(1.,0.,0.));
#11230=DIRECTION('center_axis',(0.,1.,0.));
#11231=DIRECTION('ref_axis',(1.,0.,0.));
#11232=DIRECTION('center_axis',(0.,-1.,0.));
#11233=DIRECTION('ref_axis',(1.,0.,0.));
#11234=DIRECTION('',(0.,-1.,0.));
#11235=DIRECTION('center_axis',(0.,-1.,0.));
#11236=DIRECTION('ref_axis',(1.,0.,0.));
#11237=DIRECTION('center_axis',(0.,1.,0.));
#11238=DIRECTION('ref_axis',(1.,0.,0.));
#11239=DIRECTION('center_axis',(0.,1.,0.));
#11240=DIRECTION('ref_axis',(1.,0.,0.));
#11241=DIRECTION('',(0.,-1.,0.));
#11242=DIRECTION('center_axis',(0.,1.,0.));
#11243=DIRECTION('ref_axis',(1.,0.,0.));
#11244=DIRECTION('center_axis',(0.,1.,0.));
#11245=DIRECTION('ref_axis',(1.,0.,0.));
#11246=DIRECTION('center_axis',(0.,1.,0.));
#11247=DIRECTION('ref_axis',(1.,0.,0.));
#14262=CARTESIAN_POINT('',(0.,0.,0.));
#14263=CARTESIAN_POINT('Origin',(20.,-1.8,14.));
#14264=CARTESIAN_POINT('',(19.775,-1.6,14.));
#14265=CARTESIAN_POINT('Origin',(20.,-1.6,14.));
#14266=CARTESIAN_POINT('',(19.775,-1.8,14.));
#14267=CARTESIAN_POINT('',(19.775,-1.8,14.));
#14268=CARTESIAN_POINT('Origin',(20.,-1.8,14.));
#14269=CARTESIAN_POINT('Origin',(20.,-1.8,14.));
#14270=CARTESIAN_POINT('',(19.1,-1.6,14.));
#14271=CARTESIAN_POINT('Origin',(20.,-1.6,14.));
#14272=CARTESIAN_POINT('',(19.1,-1.8,14.));
#14273=CARTESIAN_POINT('',(19.1,-1.8,14.));
#14274=CARTESIAN_POINT('Origin',(20.,-1.8,14.));
#14275=CARTESIAN_POINT('Origin',(20.,-1.6,14.));
#14276=CARTESIAN_POINT('Origin',(20.,-1.8,14.));
#14453=UNCERTAINTY_MEASURE_WITH_UNIT(LENGTH_MEASURE(0.001),#14513,
'DISTANCE_ACCURACY_VALUE',
'Maximum model space distance between geometric entities at asserted c
onnectivities');
#14455=UNCERTAINTY_MEASURE_WITH_UNIT(LENGTH_MEASURE(0.001),#14513,
'DISTANCE_ACCURACY_VALUE',
'Maximum model space distance between geometric entities at asserted c
onnectivities');
#14510=(
GEOMETRIC_REPRESENTATION_CONTEXT(3)
GLOBAL_UNCERTAINTY_ASSIGNED_CONTEXT((#14453))
GLOBAL_UNIT_ASSIGNED_CONTEXT((#14513,#14515,#14516))
REPRESENTATION_CONTEXT('','3D')
);
#14512=(
GEOMETRIC_REPRESENTATION_CONTEXT(3)
GLOBAL_UNCERTAINTY_ASSIGNED_CONTEXT((#14455))
GLOBAL_UNIT_ASSIGNED_CONTEXT((#14513,#14515,#14516))
REPRESENTATION_CONTEXT('','3D')
);
#14513=(
LENGTH_UNIT()
NAMED_UNIT(*)
SI_UNIT(.CENTI.,.METRE.)
);
#14515=(
NAMED_UNIT(*)
PLANE_ANGLE_UNIT()
SI_UNIT($,.RADIAN.)
);
#14516=(
NAMED_UNIT(*)
SI_UNIT($,.STERADIAN.)
SOLID_ANGLE_UNIT()
);
#14571=SHAPE_DEFINITION_REPRESENTATION(#14687,#14795);
#14687=PRODUCT_DEFINITION_SHAPE('',$,#14852);
#14795=SHAPE_REPRESENTATION('',(#8883),#14510);
#14797=PRODUCT_DEFINITION_CONTEXT('part definition',#14967,'design');
#14852=PRODUCT_DEFINITION('Pivot keeper (3)','Pivot keeper (3)',#14908,#14797);
#14908=PRODUCT_DEFINITION_FORMATION('',$,#15023);
#14967=APPLICATION_CONTEXT(
'Core Data for Automotive Mechanical Design Process');
#14968=PRODUCT_CONTEXT('part definition',#14967,'mechanical');
#15023=PRODUCT('Pivot keeper (3)','Pivot keeper (3)','Pivot keeper (3)',(#14968));
#15095=COLOUR_RGB('Off White',0.89,0.88,0.83);
#15096=FILL_AREA_STYLE_COLOUR('',#15095);
#15097=FILL_AREA_STYLE('',(#15096));
#15098=SURFACE_STYLE_FILL_AREA(#15097);
#15099=SURFACE_SIDE_STYLE('',(#15098));
#15100=SURFACE_STYLE_USAGE(.BOTH.,#15099);
#15101=PRESENTATION_STYLE_ASSIGNMENT((#15100));
ENDSEC;
END-ISO-10303-21;
